ISO-10303-21;
HEADER;
FILE_DESCRIPTION (('STEP AP214'),
    '1' );
FILE_NAME ('6-M6-16.step',
    '2026-10-28T16:50:19',
    ( '' ),
    ( '' ),
    'SwSTEP 2.0',
    'SolidWorks 2024',
    '' );
FILE_SCHEMA (( 'AUTOMOTIVE_DESIGN' ));
ENDSEC;

DATA;
#15=EDGE_CURVE ( 'NONE', #5505, #2772, #7117, .T. ) ;
#17=CIRCLE ( 'NONE', #5073, 3.000000000000000444 ) ;
#20=DIRECTION ( 'NONE',  ( 0.000000000000000000, 0.000000000000000000, -1.000000000000000000 ) ) ;
#38=CARTESIAN_POINT ( 'NONE',  ( 0.7500000000000000000, 2.749999999999995559, 0.000000000000000000 ) ) ;
#79=DIRECTION ( 'NONE',  ( 1.000000000000000000, 0.000000000000000000, 0.000000000000000000 ) ) ;
#112=EDGE_CURVE ( 'NONE', #6044, #3779, #6462, .T. ) ;
#119=VECTOR ( 'NONE', #1429, 1000.000000000000114 ) ;
#132=DIRECTION ( 'NONE',  ( 1.000000000000000000, 0.000000000000000000, 0.000000000000000000 ) ) ;
#150=DIRECTION ( 'NONE',  ( 0.7071067811865441310, -0.7071067811865510144, -0.000000000000000000 ) ) ;
#151=EDGE_LOOP ( 'NONE', ( #1174, #5770 ) ) ;
#167=DIRECTION ( 'NONE',  ( 0.000000000000000000, 0.000000000000000000, 1.000000000000000000 ) ) ;
#171=MANIFOLD_SOLID_BREP ( 'Pah2', #1325 ) ;
#178=LINE ( 'NONE', #891, #3319 ) ;
#200=AXIS2_PLACEMENT_3D ( 'NONE', #8510, #1928, #3508 ) ;
#203=APPLICATION_CONTEXT ( 'automotive_design' ) ;
#205=CARTESIAN_POINT ( 'NONE',  ( 0.000000000000000000, 0.000000000000000000, 21.00000000000000000 ) ) ;
#224=AXIS2_PLACEMENT_3D ( 'NONE', #4931, #4210, #2686 ) ;
#229=ORIENTED_EDGE ( 'NONE', *, *, #269, .F. ) ;
#239=CARTESIAN_POINT ( 'NONE',  ( 0.000000000000000000, 0.000000000000000000, 0.000000000000000000 ) ) ;
#244=PRODUCT_CONTEXT ( 'NONE', #4133, 'mechanical' ) ;
#263=VECTOR ( 'NONE', #2002, 1000.000000000000000 ) ;
#269=EDGE_CURVE ( 'NONE', #6362, #5838, #4273, .T. ) ;
#273=AXIS2_PLACEMENT_3D ( 'NONE', #2075, #1350, #8564 ) ;
#320=ORIENTED_EDGE ( 'NONE', *, *, #6943, .F. ) ;
#327=DIRECTION ( 'NONE',  ( -0.000000000000000000, -0.000000000000000000, -1.000000000000000000 ) ) ;
#330=LINE ( 'NONE', #4123, #7938 ) ;
#360=CARTESIAN_POINT ( 'NONE',  ( -6.000000000000000888, 0.000000000000000000, 4.000000000000000000 ) ) ;
#362=DIRECTION ( 'NONE',  ( -0.7071067811865442421, 0.7071067811865509034, 0.000000000000000000 ) ) ;
#372=CARTESIAN_POINT ( 'NONE',  ( 2.499999999999998668, 3.061616997868381662E-16, 21.00000000000000000 ) ) ;
#396=ADVANCED_FACE ( 'NONE', ( #2058, #4983 ), #8012, .T. ) ;
#408=EDGE_LOOP ( 'NONE', ( #6150, #3205, #7660, #2925 ) ) ;
#411=VECTOR ( 'NONE', #1740, 1000.000000000000000 ) ;
#417=AXIS2_PLACEMENT_3D ( 'NONE', #8112, #7380, #7479 ) ;
#430=DIRECTION ( 'NONE',  ( 0.000000000000000000, -0.000000000000000000, -1.000000000000000000 ) ) ;
#457=DIRECTION ( 'NONE',  ( 0.000000000000000000, 0.000000000000000000, 1.000000000000000000 ) ) ;
#482=ORIENTED_EDGE ( 'NONE', *, *, #2518, .F. ) ;
#487=DIRECTION ( 'NONE',  ( 0.000000000000000000, 0.000000000000000000, 1.000000000000000000 ) ) ;
#511=ADVANCED_FACE ( 'NONE', ( #5806 ), #9311, .T. ) ;
#514=ORIENTED_EDGE ( 'NONE', *, *, #8952, .T. ) ;
#519=FACE_OUTER_BOUND ( 'NONE', #8224, .T. ) ;
#531=FACE_OUTER_BOUND ( 'NONE', #7505, .T. ) ;
#532=ADVANCED_FACE ( 'NONE', ( #1086 ), #4027, .T. ) ;
#538=CARTESIAN_POINT ( 'NONE',  ( 0.7500000000000000000, -0.7500000000000000000, 1.500000000000000000 ) ) ;
#562=VECTOR ( 'NONE', #7217, 1000.000000000000000 ) ;
#567=VECTOR ( 'NONE', #150, 999.9999999999998863 ) ;
#581=DIRECTION ( 'NONE',  ( -0.7071067811865505703, -0.7071067811865444641, 0.000000000000000000 ) ) ;
#599=ADVANCED_FACE ( 'NONE', ( #4699 ), #7576, .T. ) ;
#605=DIRECTION ( 'NONE',  ( 0.000000000000000000, 0.000000000000000000, 1.000000000000000000 ) ) ;
#610=AXIS2_PLACEMENT_3D ( 'NONE', #5055, #7982, #487 ) ;
#619=ADVANCED_FACE ( 'NONE', ( #5567 ), #6285, .T. ) ;
#623=CARTESIAN_POINT ( 'NONE',  ( 5.000000000000000888, 0.000000000000000000, 1.000000000000000000 ) ) ;
#635=ORIENTED_EDGE ( 'NONE', *, *, #1121, .F. ) ;
#639=PLANE ( 'NONE',  #3264 ) ;
#654=CARTESIAN_POINT ( 'NONE',  ( 1.749999999999997780, -1.750000000000013101, 0.000000000000000000 ) ) ;
#664=VECTOR ( 'NONE', #7045, 1000.000000000000000 ) ;
#674=DIRECTION ( 'NONE',  ( 0.7071067811865441310, -0.7071067811865510144, 0.000000000000000000 ) ) ;
#701=LINE ( 'NONE', #751, #6370 ) ;
#702=CARTESIAN_POINT ( 'NONE',  ( 2.749999999999996447, -0.7500000000000000000, 1.500000000000000000 ) ) ;
#734=AXIS2_PLACEMENT_3D ( 'NONE', #7960, #4205, #1319 ) ;
#751=CARTESIAN_POINT ( 'NONE',  ( -2.749999999999995559, 0.7500000000000000000, 1.500000000000000000 ) ) ;
#760=CARTESIAN_POINT ( 'NONE',  ( 0.7500000000000000000, 0.7500000000000000000, 1.500000000000000000 ) ) ;
#763=VERTEX_POINT ( 'NONE', #1956 ) ;
#764=ORIENTED_EDGE ( 'NONE', *, *, #2101, .T. ) ;
#768=CARTESIAN_POINT ( 'NONE',  ( 0.7500000000000000000, 0.7500000000000000000, 1.500000000000000000 ) ) ;
#775=ORIENTED_EDGE ( 'NONE', *, *, #3550, .T. ) ;
#776=CARTESIAN_POINT ( 'NONE',  ( 2.749999999999996447, -0.7500000000000000000, 0.000000000000000000 ) ) ;
#780=CARTESIAN_POINT ( 'NONE',  ( 0.000000000000000000, 0.000000000000000000, 5.000000000000000000 ) ) ;
#784=ORIENTED_EDGE ( 'NONE', *, *, #3601, .F. ) ;
#785=ORIENTED_EDGE ( 'NONE', *, *, #4032, .T. ) ;
#796=CARTESIAN_POINT ( 'NONE',  ( -0.7500000000000000000, -0.7500000000000000000, 1.500000000000000000 ) ) ;
#806=ORIENTED_EDGE ( 'NONE', *, *, #8639, .T. ) ;
#841=EDGE_CURVE ( 'NONE', #3430, #5108, #5965, .T. ) ;
#878=DIRECTION ( 'NONE',  ( 0.000000000000000000, 1.000000000000000000, 0.000000000000000000 ) ) ;
#880=CARTESIAN_POINT ( 'NONE',  ( -3.500000000000000000, 2.818925648462311528E-15, 0.000000000000000000 ) ) ;
#882=ORIENTED_EDGE ( 'NONE', *, *, #4636, .F. ) ;
#891=CARTESIAN_POINT ( 'NONE',  ( 0.7500000000000000000, 0.7500000000000000000, 1.500000000000000000 ) ) ;
#906=TOROIDAL_SURFACE ( 'NONE', #4897, 5.000000000000000888, 1.000000000000000000 ) ;
#912=SHAPE_DEFINITION_REPRESENTATION ( #7841, #8501 ) ;
#916=CARTESIAN_POINT ( 'NONE',  ( -3.000000000000000444, 0.000000000000000000, 5.000000000000000000 ) ) ;
#931=ORIENTED_EDGE ( 'NONE', *, *, #8715, .T. ) ;
#950=EDGE_CURVE ( 'NONE', #8301, #4792, #3047, .T. ) ;
#956=VERTEX_POINT ( 'NONE', #1660 ) ;
#970=LINE ( 'NONE', #6793, #5257 ) ;
#989=EDGE_LOOP ( 'NONE', ( #1864, #1558 ) ) ;
#990=DIRECTION ( 'NONE',  ( 0.000000000000000000, 0.000000000000000000, 1.000000000000000000 ) ) ;
#991=VERTEX_POINT ( 'NONE', #4541 ) ;
#1012=CARTESIAN_POINT ( 'NONE',  ( 0.7500000000000000000, 2.749999999999995559, 1.500000000000000000 ) ) ;
#1014=ORIENTED_EDGE ( 'NONE', *, *, #2234, .T. ) ;
#1020=DIRECTION ( 'NONE',  ( 1.000000000000000000, 0.000000000000000000, 0.000000000000000000 ) ) ;
#1030=DIRECTION ( 'NONE',  ( 0.000000000000000000, -0.000000000000000000, 1.000000000000000000 ) ) ;
#1040=ORIENTED_EDGE ( 'NONE', *, *, #1125, .F. ) ;
#1044=DIRECTION ( 'NONE',  ( -0.7071067811865444641, 0.7071067811865505703, 0.000000000000000000 ) ) ;
#1048=CARTESIAN_POINT ( 'NONE',  ( 0.7500000000000000000, 0.7500000000000000000, 0.000000000000000000 ) ) ;
#1062=DIRECTION ( 'NONE',  ( 1.000000000000000000, 0.000000000000000000, 0.000000000000000000 ) ) ;
#1077=LINE ( 'NONE', #6141, #5103 ) ;
#1086=FACE_OUTER_BOUND ( 'NONE', #9186, .T. ) ;
#1090=LINE ( 'NONE', #4611, #8857 ) ;
#1096=CARTESIAN_POINT ( 'NONE',  ( -2.749999999999995559, 0.7500000000000000000, 0.000000000000000000 ) ) ;
#1103=CARTESIAN_POINT ( 'NONE',  ( 2.750000000000006661, 0.7500000000000000000, 1.500000000000000000 ) ) ;
#1105=ORIENTED_EDGE ( 'NONE', *, *, #841, .T. ) ;
#1112=DIRECTION ( 'NONE',  ( 1.000000000000000000, 0.000000000000000000, 0.000000000000000000 ) ) ;
#1121=EDGE_CURVE ( 'NONE', #2334, #6860, #2166, .T. ) ;
#1125=EDGE_CURVE ( 'NONE', #3327, #6611, #5517, .T. ) ;
#1146=LINE ( 'NONE', #6972, #1344 ) ;
#1174=ORIENTED_EDGE ( 'NONE', *, *, #7702, .T. ) ;
#1213=ORIENTED_EDGE ( 'NONE', *, *, #6366, .F. ) ;
#1215=LINE ( 'NONE', #1358, #562 ) ;
#1250=ADVANCED_FACE ( 'NONE', ( #3131 ), #906, .T. ) ;
#1273=ADVANCED_FACE ( 'NONE', ( #8981 ), #1734, .T. ) ;
#1285=ORIENTED_EDGE ( 'NONE', *, *, #4216, .F. ) ;
#1319=DIRECTION ( 'NONE',  ( -1.000000000000000000, 1.224646799147353454E-16, 0.000000000000000000 ) ) ;
#1325=CLOSED_SHELL ( 'NONE', ( #9219, #1250, #511, #3300, #532, #4442, #396, #7245, #8155, #1469, #4846, #3506, #619, #3243, #5676, #7534, #7289, #8858, #1454, #2663, #4713, #5237, #8409, #1273, #4731, #7646, #599, #5301, #5182, #2175 ) ) ;
#1335=EDGE_CURVE ( 'NONE', #4792, #3327, #7628, .T. ) ;
#1336=AXIS2_PLACEMENT_3D ( 'NONE', #239, #3014, #3162 ) ;
#1337=DIRECTION ( 'NONE',  ( 0.000000000000000000, 0.000000000000000000, 1.000000000000000000 ) ) ;
#1344=VECTOR ( 'NONE', #7015, 1000.000000000000114 ) ;
#1350=DIRECTION ( 'NONE',  ( -1.000000000000000000, 0.000000000000000000, 0.000000000000000000 ) ) ;
#1358=CARTESIAN_POINT ( 'NONE',  ( -3.000000000000000444, 0.000000000000000000, 21.00000000000000000 ) ) ;
#1367=CARTESIAN_POINT ( 'NONE',  ( 0.7500000000000000000, 0.7500000000000000000, 0.000000000000000000 ) ) ;
#1403=PLANE ( 'NONE',  #5641 ) ;
#1409=ORIENTED_EDGE ( 'NONE', *, *, #7594, .T. ) ;
#1429=DIRECTION ( 'NONE',  ( 0.7071067811865441310, -0.7071067811865507924, -0.000000000000000000 ) ) ;
#1434=VERTEX_POINT ( 'NONE', #4087 ) ;
#1444=CARTESIAN_POINT ( 'NONE',  ( 0.000000000000000000, 0.000000000000000000, 1.000000000000000000 ) ) ;
#1453=DIRECTION ( 'NONE',  ( -1.000000000000000000, 0.000000000000000000, 0.000000000000000000 ) ) ;
#1454=ADVANCED_FACE ( 'NONE', ( #6308 ), #9213, .F. ) ;
#1458=ORIENTED_EDGE ( 'NONE', *, *, #2101, .F. ) ;
#1466=DIRECTION ( 'NONE',  ( 1.000000000000000000, 0.000000000000000000, -0.000000000000000000 ) ) ;
#1469=ADVANCED_FACE ( 'NONE', ( #7921 ), #7785, .T. ) ;
#1495=AXIS2_PLACEMENT_3D ( 'NONE', #1929, #5636, #4094 ) ;
#1503=CYLINDRICAL_SURFACE ( 'NONE', #7807, 6.000000000000000888 ) ;
#1507=ORIENTED_EDGE ( 'NONE', *, *, #5423, .F. ) ;
#1521=ORIENTED_EDGE ( 'NONE', *, *, #7864, .T. ) ;
#1532=EDGE_CURVE ( 'NONE', #4339, #5838, #2201, .T. ) ;
#1537=CARTESIAN_POINT ( 'NONE',  ( -2.749999999999995559, 0.7500000000000000000, 1.500000000000000000 ) ) ;
#1540=CARTESIAN_POINT ( 'NONE',  ( -0.7500000000000000000, 2.750000000000002665, 1.500000000000000000 ) ) ;
#1558=ORIENTED_EDGE ( 'NONE', *, *, #841, .F. ) ;
#1580=ORIENTED_EDGE ( 'NONE', *, *, #3127, .F. ) ;
#1589=EDGE_CURVE ( 'NONE', #2537, #2280, #3787, .T. ) ;
#1597=EDGE_LOOP ( 'NONE', ( #6253, #4748, #1285, #3156 ) ) ;
#1600=CARTESIAN_POINT ( 'NONE',  ( -0.7500000000000000000, 0.7500000000000000000, 1.500000000000000000 ) ) ;
#1608=CARTESIAN_POINT ( 'NONE',  ( 0.000000000000000000, 0.000000000000000000, 0.000000000000000000 ) ) ;
#1614=AXIS2_PLACEMENT_3D ( 'NONE', #6760, #5504, #4539 ) ;
#1617=LINE ( 'NONE', #5275, #3582 ) ;
#1619=ORIENTED_EDGE ( 'NONE', *, *, #8715, .F. ) ;
#1621=LINE ( 'NONE', #2398, #5183 ) ;
#1660=CARTESIAN_POINT ( 'NONE',  ( 6.000000000000000888, 7.347880794884120722E-16, 4.000000000000000000 ) ) ;
#1663=EDGE_CURVE ( 'NONE', #5576, #6611, #1090, .T. ) ;
#1667=PLANE ( 'NONE',  #6673 ) ;
#1669=ORIENTED_EDGE ( 'NONE', *, *, #4554, .T. ) ;
#1702=EDGE_LOOP ( 'NONE', ( #3929, #6032 ) ) ;
#1709=DIRECTION ( 'NONE',  ( 0.000000000000000000, 0.000000000000000000, -1.000000000000000000 ) ) ;
#1711=DIRECTION ( 'NONE',  ( -0.7071067811865505703, -0.7071067811865444641, -0.000000000000000000 ) ) ;
#1726=ORIENTED_EDGE ( 'NONE', *, *, #4554, .F. ) ;
#1730=CARTESIAN_POINT ( 'NONE',  ( 0.7500000000000000000, 2.749999999999995559, 0.000000000000000000 ) ) ;
#1732=CARTESIAN_POINT ( 'NONE',  ( -0.7500000000000000000, -2.749999999999995559, 0.000000000000000000 ) ) ;
#1733=AXIS2_PLACEMENT_3D ( 'NONE', #3285, #8331, #2387 ) ;
#1734=PLANE ( 'NONE',  #8430 ) ;
#1740=DIRECTION ( 'NONE',  ( 0.000000000000000000, 0.000000000000000000, -1.000000000000000000 ) ) ;
#1742=PLANE ( 'NONE',  #9196 ) ;
#1754=DIRECTION ( 'NONE',  ( -1.000000000000000000, -0.000000000000000000, -0.000000000000000000 ) ) ;
#1763=ORIENTED_EDGE ( 'NONE', *, *, #7594, .F. ) ;
#1765=CARTESIAN_POINT ( 'NONE',  ( 3.000000000000000444, 3.673940397442060361E-16, 21.00000000000000000 ) ) ;
#1787=LINE ( 'NONE', #6276, #6440 ) ;
#1800=AXIS2_PLACEMENT_3D ( 'NONE', #2797, #9319, #7028 ) ;
#1806=EDGE_CURVE ( 'NONE', #5838, #9262, #7057, .T. ) ;
#1811=ORIENTED_EDGE ( 'NONE', *, *, #5416, .F. ) ;
#1836=EDGE_CURVE ( 'NONE', #5958, #6044, #9444, .T. ) ;
#1864=ORIENTED_EDGE ( 'NONE', *, *, #4032, .F. ) ;
#1874=DIRECTION ( 'NONE',  ( 0.000000000000000000, 0.000000000000000000, 1.000000000000000000 ) ) ;
#1878=VECTOR ( 'NONE', #3275, 1000.000000000000000 ) ;
#1879=ORIENTED_EDGE ( 'NONE', *, *, #1663, .T. ) ;
#1882=LINE ( 'NONE', #5731, #5573 ) ;
#1909=EDGE_LOOP ( 'NONE', ( #9309, #2793, #5362, #635 ) ) ;
#1918=ORIENTED_EDGE ( 'NONE', *, *, #6530, .F. ) ;
#1920=PLANE ( 'NONE',  #8048 ) ;
#1928=DIRECTION ( 'NONE',  ( 0.000000000000000000, -1.000000000000000000, 0.000000000000000000 ) ) ;
#1929=CARTESIAN_POINT ( 'NONE',  ( 0.000000000000000000, 0.000000000000000000, 4.000000000000000000 ) ) ;
#1937=AXIS2_PLACEMENT_3D ( 'NONE', #1537, #674, #2886 ) ;
#1956=CARTESIAN_POINT ( 'NONE',  ( -4.119968255444916849E-15, -3.500000000000000000, 1.500000000000000000 ) ) ;
#1957=EDGE_CURVE ( 'NONE', #6427, #8186, #1617, .T. ) ;
#1982=DIRECTION ( 'NONE',  ( -0.7071067811865444641, 0.7071067811865505703, -0.000000000000000000 ) ) ;
#1998=CARTESIAN_POINT ( 'NONE',  ( -0.7500000000000000000, 0.7500000000000000000, 1.500000000000000000 ) ) ;
#2002=DIRECTION ( 'NONE',  ( -1.000000000000000000, 0.000000000000000000, 0.000000000000000000 ) ) ;
#2058=FACE_OUTER_BOUND ( 'NONE', #151, .T. ) ;
#2063=CARTESIAN_POINT ( 'NONE',  ( 0.7500000000000000000, -0.7500000000000000000, 1.500000000000000000 ) ) ;
#2071=CARTESIAN_POINT ( 'NONE',  ( 0.7500000000000000000, 0.7500000000000000000, 1.500000000000000000 ) ) ;
#2075=CARTESIAN_POINT ( 'NONE',  ( -0.7500000000000000000, 0.7500000000000000000, 1.500000000000000000 ) ) ;
#2082=PLANE ( 'NONE',  #5291 ) ;
#2101=EDGE_CURVE ( 'NONE', #2895, #8186, #9099, .T. ) ;
#2103=VECTOR ( 'NONE', #6487, 1000.000000000000000 ) ;
#2127=EDGE_CURVE ( 'NONE', #2772, #6441, #2770, .T. ) ;
#2136=ORIENTED_EDGE ( 'NONE', *, *, #1836, .T. ) ;
#2159=VERTEX_POINT ( 'NONE', #5654 ) ;
#2166=LINE ( 'NONE', #5295, #6591 ) ;
#2170=ORIENTED_EDGE ( 'NONE', *, *, #8695, .F. ) ;
#2175=ADVANCED_FACE ( 'NONE', ( #4921 ), #6994, .T. ) ;
#2178=ORIENTED_EDGE ( 'NONE', *, *, #4216, .T. ) ;
#2201=LINE ( 'NONE', #3074, #9300 ) ;
#2224=EDGE_LOOP ( 'NONE', ( #2611, #8669 ) ) ;
#2227=ORIENTED_EDGE ( 'NONE', *, *, #6711, .T. ) ;
#2234=EDGE_CURVE ( 'NONE', #2537, #2895, #7128, .T. ) ;
#2252=ORIENTED_EDGE ( 'NONE', *, *, #5423, .T. ) ;
#2261=PLANE ( 'NONE',  #1937 ) ;
#2265=CARTESIAN_POINT ( 'NONE',  ( 0.7500000000000000000, 0.7500000000000000000, 0.000000000000000000 ) ) ;
#2268=DIRECTION ( 'NONE',  ( -0.000000000000000000, -0.000000000000000000, -1.000000000000000000 ) ) ;
#2275=DIRECTION ( 'NONE',  ( 0.000000000000000000, -0.000000000000000000, 1.000000000000000000 ) ) ;
#2280=VERTEX_POINT ( 'NONE', #2370 ) ;
#2297=CARTESIAN_POINT ( 'NONE',  ( -3.500000000000000000, 4.119968255444916849E-15, 1.500000000000000000 ) ) ;
#2326=CARTESIAN_POINT ( 'NONE',  ( 0.000000000000000000, 0.000000000000000000, 0.000000000000000000 ) ) ;
#2334=VERTEX_POINT ( 'NONE', #4766 ) ;
#2338=CARTESIAN_POINT ( 'NONE',  ( 0.000000000000000000, 0.000000000000000000, 5.000000000000000000 ) ) ;
#2363=CARTESIAN_POINT ( 'NONE',  ( 0.7500000000000000000, 0.7500000000000000000, 1.500000000000000000 ) ) ;
#2370=CARTESIAN_POINT ( 'NONE',  ( 0.7500000000000000000, 2.749999999999995559, 1.500000000000000000 ) ) ;
#2381=CIRCLE ( 'NONE', #2978, 1.000000000000000000 ) ;
#2387=DIRECTION ( 'NONE',  ( -1.000000000000000000, 1.224646799147353454E-16, 0.000000000000000000 ) ) ;
#2398=CARTESIAN_POINT ( 'NONE',  ( 6.000000000000000888, 7.347880794884120722E-16, 5.000000000000000000 ) ) ;
#2405=VECTOR ( 'NONE', #6335, 1000.000000000000000 ) ;
#2406=VERTEX_POINT ( 'NONE', #1103 ) ;
#2414=DIRECTION ( 'NONE',  ( -0.7071067811865510144, -0.7071067811865441310, 0.000000000000000000 ) ) ;
#2416=VECTOR ( 'NONE', #6409, 1000.000000000000000 ) ;
#2426=VECTOR ( 'NONE', #5054, 1000.000000000000000 ) ;
#2436=( LENGTH_UNIT ( ) NAMED_UNIT ( * ) SI_UNIT ( .MILLI., .METRE. ) );
#2455=ORIENTED_EDGE ( 'NONE', *, *, #112, .T. ) ;
#2474=CARTESIAN_POINT ( 'NONE',  ( 3.500000000000000444, -6.505213034913026604E-16, 0.000000000000000000 ) ) ;
#2500=DIRECTION ( 'NONE',  ( 0.7071067811865460184, 8.659560562354913137E-17, -0.7071067811865489050 ) ) ;
#2508=DIRECTION ( 'NONE',  ( -0.7071067811865441310, 0.7071067811865510144, -0.000000000000000000 ) ) ;
#2511=ORIENTED_EDGE ( 'NONE', *, *, #9181, .T. ) ;
#2512=CARTESIAN_POINT ( 'NONE',  ( -3.500000000000000000, 4.119968255444916849E-15, 0.000000000000000000 ) ) ;
#2518=EDGE_CURVE ( 'NONE', #2159, #6631, #8636, .T. ) ;
#2520=ORIENTED_EDGE ( 'NONE', *, *, #1589, .F. ) ;
#2527=DIRECTION ( 'NONE',  ( 0.7071067811865507924, 0.7071067811865441310, -0.000000000000000000 ) ) ;
#2528=CIRCLE ( 'NONE', #224, 3.000000000000000444 ) ;
#2537=VERTEX_POINT ( 'NONE', #7830 ) ;
#2565=FACE_OUTER_BOUND ( 'NONE', #1909, .T. ) ;
#2566=CARTESIAN_POINT ( 'NONE',  ( 0.7500000000000000000, -0.7500000000000000000, 0.000000000000000000 ) ) ;
#2584=VERTEX_POINT ( 'NONE', #7150 ) ;
#2586=CARTESIAN_POINT ( 'NONE',  ( -2.750000000000002665, -0.7500000000000000000, 0.000000000000000000 ) ) ;
#2591=EDGE_LOOP ( 'NONE', ( #882, #5563, #8324, #7902 ) ) ;
#2593=VECTOR ( 'NONE', #7371, 1000.000000000000000 ) ;
#2602=CARTESIAN_POINT ( 'NONE',  ( 3.500000000000000444, -2.818925648462311528E-15, 0.000000000000000000 ) ) ;
#2604=EDGE_CURVE ( 'NONE', #8987, #6860, #2920, .T. ) ;
#2611=ORIENTED_EDGE ( 'NONE', *, *, #3601, .T. ) ;
#2619=ORIENTED_EDGE ( 'NONE', *, *, #7810, .F. ) ;
#2642=DIRECTION ( 'NONE',  ( 1.000000000000000000, -0.000000000000000000, -0.000000000000000000 ) ) ;
#2645=EDGE_LOOP ( 'NONE', ( #3021, #5451, #1726, #6636 ) ) ;
#2653=DIRECTION ( 'NONE',  ( 0.000000000000000000, -1.000000000000000000, 0.000000000000000000 ) ) ;
#2658=PLANE ( 'NONE',  #200 ) ;
#2663=ADVANCED_FACE ( 'NONE', ( #8066 ), #4416, .F. ) ;
#2675=DIRECTION ( 'NONE',  ( 0.000000000000000000, -1.000000000000000000, 0.000000000000000000 ) ) ;
#2680=CARTESIAN_POINT ( 'NONE',  ( 0.000000000000000000, 0.000000000000000000, 4.000000000000000000 ) ) ;
#2682=CARTESIAN_POINT ( 'NONE',  ( -0.7500000000000000000, -0.7500000000000000000, 0.000000000000000000 ) ) ;
#2683=VECTOR ( 'NONE', #3152, 1000.000000000000000 ) ;
#2685=VECTOR ( 'NONE', #8053, 1000.000000000000000 ) ;
#2686=DIRECTION ( 'NONE',  ( 1.000000000000000000, 0.000000000000000000, 0.000000000000000000 ) ) ;
#2697=VERTEX_POINT ( 'NONE', #7434 ) ;
#2722=EDGE_LOOP ( 'NONE', ( #1918, #2252, #4757, #785 ) ) ;
#2723=AXIS2_PLACEMENT_3D ( 'NONE', #2063, #2653, #4854 ) ;
#2724=EDGE_LOOP ( 'NONE', ( #7156, #3318, #2511, #1507 ) ) ;
#2726=( GEOMETRIC_REPRESENTATION_CONTEXT ( 3 ) GLOBAL_UNCERTAINTY_ASSIGNED_CONTEXT ( ( #7486 ) ) GLOBAL_UNIT_ASSIGNED_CONTEXT ( ( #3038, #6790, #5976 ) ) REPRESENTATION_CONTEXT ( 'NONE', 'WORKASPACE' ) );
#2742=VECTOR ( 'NONE', #7286, 1000.000000000000000 ) ;
#2770=LINE ( 'NONE', #8486, #7735 ) ;
#2772=VERTEX_POINT ( 'NONE', #6247 ) ;
#2793=ORIENTED_EDGE ( 'NONE', *, *, #7323, .T. ) ;
#2797=CARTESIAN_POINT ( 'NONE',  ( 0.000000000000000000, 0.000000000000000000, 5.000000000000000000 ) ) ;
#2829=FACE_OUTER_BOUND ( 'NONE', #7753, .T. ) ;
#2848=EDGE_CURVE ( 'NONE', #2860, #3262, #2528, .T. ) ;
#2853=ORIENTED_EDGE ( 'NONE', *, *, #7954, .T. ) ;
#2860=VERTEX_POINT ( 'NONE', #4077 ) ;
#2875=AXIS2_PLACEMENT_3D ( 'NONE', #623, #5768, #4944 ) ;
#2886=DIRECTION ( 'NONE',  ( 0.000000000000000000, 0.000000000000000000, 1.000000000000000000 ) ) ;
#2887=VECTOR ( 'NONE', #2508, 999.9999999999998863 ) ;
#2893=FACE_OUTER_BOUND ( 'NONE', #7695, .T. ) ;
#2895=VERTEX_POINT ( 'NONE', #9351 ) ;
#2909=DIRECTION ( 'NONE',  ( 1.000000000000000000, 0.000000000000000000, 0.000000000000000000 ) ) ;
#2913=CARTESIAN_POINT ( 'NONE',  ( 3.500000000000000444, -6.505213034913026604E-16, 1.500000000000000000 ) ) ;
#2919=EDGE_CURVE ( 'NONE', #4339, #6427, #7056, .T. ) ;
#2920=LINE ( 'NONE', #6005, #6054 ) ;
#2925=ORIENTED_EDGE ( 'NONE', *, *, #112, .F. ) ;
#2928=ORIENTED_EDGE ( 'NONE', *, *, #4131, .F. ) ;
#2953=LINE ( 'NONE', #4542, #2593 ) ;
#2978=AXIS2_PLACEMENT_3D ( 'NONE', #5220, #4599, #8961 ) ;
#2996=ORIENTED_EDGE ( 'NONE', *, *, #1589, .T. ) ;
#3014=DIRECTION ( 'NONE',  ( -0.000000000000000000, -0.000000000000000000, -1.000000000000000000 ) ) ;
#3021=ORIENTED_EDGE ( 'NONE', *, *, #1957, .T. ) ;
#3038=( LENGTH_UNIT ( ) NAMED_UNIT ( * ) SI_UNIT ( .MILLI., .METRE. ) );
#3045=VECTOR ( 'NONE', #1030, 1000.000000000000000 ) ;
#3047=CIRCLE ( 'NONE', #4890, 5.000000000000000888 ) ;
#3074=CARTESIAN_POINT ( 'NONE',  ( -1.749999999999984235, 1.750000000000001554, 0.000000000000000000 ) ) ;
#3080=DIRECTION ( 'NONE',  ( 1.000000000000000000, 0.000000000000000000, 0.000000000000000000 ) ) ;
#3110=DIRECTION ( 'NONE',  ( 1.000000000000000000, 0.000000000000000000, 0.000000000000000000 ) ) ;
#3118=DIRECTION ( 'NONE',  ( -0.000000000000000000, -0.000000000000000000, -1.000000000000000000 ) ) ;
#3127=EDGE_CURVE ( 'NONE', #2334, #3397, #5221, .T. ) ;
#3128=EDGE_CURVE ( 'NONE', #6362, #8767, #701, .T. ) ;
#3131=FACE_OUTER_BOUND ( 'NONE', #8282, .T. ) ;
#3152=DIRECTION ( 'NONE',  ( 0.000000000000000000, 0.000000000000000000, 1.000000000000000000 ) ) ;
#3156=ORIENTED_EDGE ( 'NONE', *, *, #7323, .F. ) ;
#3162=DIRECTION ( 'NONE',  ( 1.000000000000000000, 0.000000000000000000, 0.000000000000000000 ) ) ;
#3182=TOROIDAL_SURFACE ( 'NONE', #4406, 5.000000000000000888, 1.000000000000000000 ) ;
#3183=DIRECTION ( 'NONE',  ( 1.000000000000000000, 0.000000000000000000, -0.000000000000000000 ) ) ;
#3198=DIRECTION ( 'NONE',  ( -0.000000000000000000, -0.000000000000000000, -1.000000000000000000 ) ) ;
#3200=DIRECTION ( 'NONE',  ( 0.7071067811865441310, -0.7071067811865510144, -0.000000000000000000 ) ) ;
#3205=ORIENTED_EDGE ( 'NONE', *, *, #8629, .T. ) ;
#3231=DIRECTION ( 'NONE',  ( -0.7071067811865441310, 0.7071067811865507924, -0.000000000000000000 ) ) ;
#3243=ADVANCED_FACE ( 'NONE', ( #8657 ), #6503, .F. ) ;
#3248=DIRECTION ( 'NONE',  ( 0.000000000000000000, 1.000000000000000000, 0.000000000000000000 ) ) ;
#3262=VERTEX_POINT ( 'NONE', #5057 ) ;
#3264=AXIS2_PLACEMENT_3D ( 'NONE', #2326, #6214, #3183 ) ;
#3275=DIRECTION ( 'NONE',  ( 0.000000000000000000, 0.000000000000000000, -1.000000000000000000 ) ) ;
#3285=CARTESIAN_POINT ( 'NONE',  ( -5.000000000000000888, 6.123233995736767268E-16, 1.000000000000000000 ) ) ;
#3300=ADVANCED_FACE ( 'NONE', ( #2893 ), #8750, .T. ) ;
#3318=ORIENTED_EDGE ( 'NONE', *, *, #6259, .F. ) ;
#3319=VECTOR ( 'NONE', #79, 1000.000000000000000 ) ;
#3327=VERTEX_POINT ( 'NONE', #4432 ) ;
#3360=AXIS2_PLACEMENT_3D ( 'NONE', #1444, #6642, #5097 ) ;
#3381=LINE ( 'NONE', #6286, #9209 ) ;
#3397=VERTEX_POINT ( 'NONE', #8133 ) ;
#3403=DIRECTION ( 'NONE',  ( 0.000000000000000000, 0.000000000000000000, 1.000000000000000000 ) ) ;
#3420=ORIENTED_EDGE ( 'NONE', *, *, #5342, .T. ) ;
#3430=VERTEX_POINT ( 'NONE', #5766 ) ;
#3443=AXIS2_PLACEMENT_3D ( 'NONE', #7782, #1874, #1466 ) ;
#3465=ORIENTED_EDGE ( 'NONE', *, *, #1806, .T. ) ;
#3479=EDGE_LOOP ( 'NONE', ( #2227, #2996, #8265, #5805, #775, #2136, #4292, #8253, #3615, #4612, #4371, #7877, #931, #8734, #1409, #1669 ) ) ;
#3480=AXIS2_PLACEMENT_3D ( 'NONE', #5240, #9463, #5093 ) ;
#3487=CIRCLE ( 'NONE', #1495, 6.000000000000000888 ) ;
#3500=ORIENTED_EDGE ( 'NONE', *, *, #7864, .F. ) ;
#3506=ADVANCED_FACE ( 'NONE', ( #2829 ), #3182, .T. ) ;
#3507=AXIS2_PLACEMENT_3D ( 'NONE', #7556, #9132, #1112 ) ;
#3508=DIRECTION ( 'NONE',  ( 0.000000000000000000, -0.000000000000000000, -1.000000000000000000 ) ) ;
#3545=VERTEX_POINT ( 'NONE', #8736 ) ;
#3550=EDGE_CURVE ( 'NONE', #2406, #5958, #9406, .T. ) ;
#3582=VECTOR ( 'NONE', #3248, 1000.000000000000000 ) ;
#3601=EDGE_CURVE ( 'NONE', #4792, #8301, #6272, .T. ) ;
#3615=ORIENTED_EDGE ( 'NONE', *, *, #7515, .T. ) ;
#3625=ORIENTED_EDGE ( 'NONE', *, *, #8952, .F. ) ;
#3634=DIRECTION ( 'NONE',  ( 0.7071067811865510144, 0.7071067811865441310, -0.000000000000000000 ) ) ;
#3639=ORIENTED_EDGE ( 'NONE', *, *, #8909, .F. ) ;
#3672=DIRECTION ( 'NONE',  ( -0.000000000000000000, -0.000000000000000000, -1.000000000000000000 ) ) ;
#3681=CARTESIAN_POINT ( 'NONE',  ( 2.750000000000006661, 0.7500000000000000000, 1.500000000000000000 ) ) ;
#3700=DIRECTION ( 'NONE',  ( -0.000000000000000000, -0.000000000000000000, -1.000000000000000000 ) ) ;
#3701=ADVANCED_BREP_SHAPE_REPRESENTATION ( '', ( #171, #1614 ), #6385 ) ;
#3729=DIRECTION ( 'NONE',  ( 0.7071067811865510144, 0.7071067811865441310, -0.000000000000000000 ) ) ;
#3731=EDGE_CURVE ( 'NONE', #763, #991, #330, .T. ) ;
#3747=LINE ( 'NONE', #7349, #8683 ) ;
#3755=VERTEX_POINT ( 'NONE', #1048 ) ;
#3775=CARTESIAN_POINT ( 'NONE',  ( 0.000000000000000000, 0.000000000000000000, 1.000000000000000000 ) ) ;
#3779=VERTEX_POINT ( 'NONE', #6198 ) ;
#3787=LINE ( 'NONE', #6677, #567 ) ;
#3801=AXIS2_PLACEMENT_3D ( 'NONE', #4697, #990, #3110 ) ;
#3804=ORIENTED_EDGE ( 'NONE', *, *, #2919, .T. ) ;
#3828=EDGE_CURVE ( 'NONE', #2159, #3262, #6155, .T. ) ;
#3866=DIRECTION ( 'NONE',  ( -0.000000000000000000, -0.000000000000000000, -1.000000000000000000 ) ) ;
#3872=LINE ( 'NONE', #8868, #2683 ) ;
#3891=DIRECTION ( 'NONE',  ( 0.000000000000000000, 0.000000000000000000, 1.000000000000000000 ) ) ;
#3911=ORIENTED_EDGE ( 'NONE', *, *, #8006, .F. ) ;
#3929=ORIENTED_EDGE ( 'NONE', *, *, #6259, .T. ) ;
#3935=VECTOR ( 'NONE', #4665, 1000.000000000000000 ) ;
#3946=AXIS2_PLACEMENT_3D ( 'NONE', #4137, #3403, #6347 ) ;
#3984=DIRECTION ( 'NONE',  ( 0.000000000000000000, 0.000000000000000000, 1.000000000000000000 ) ) ;
#3985=VECTOR ( 'NONE', #878, 1000.000000000000000 ) ;
#3987=EDGE_LOOP ( 'NONE', ( #7205, #8456, #1811, #3500 ) ) ;
#3997=LINE ( 'NONE', #6165, #2887 ) ;
#4027=CYLINDRICAL_SURFACE ( 'NONE', #5739, 6.000000000000000888 ) ;
#4032=EDGE_CURVE ( 'NONE', #5108, #3430, #17, .T. ) ;
#4040=DIRECTION ( 'NONE',  ( 1.000000000000000000, 0.000000000000000000, 0.000000000000000000 ) ) ;
#4074=CARTESIAN_POINT ( 'NONE',  ( 0.000000000000000000, 0.000000000000000000, 5.000000000000000000 ) ) ;
#4077=CARTESIAN_POINT ( 'NONE',  ( -3.000000000000000444, 0.000000000000000000, 20.49999999999999645 ) ) ;
#4087=CARTESIAN_POINT ( 'NONE',  ( 5.000000000000000888, 0.000000000000000000, 5.000000000000000000 ) ) ;
#4091=VECTOR ( 'NONE', #2527, 1000.000000000000114 ) ;
#4094=DIRECTION ( 'NONE',  ( 1.000000000000000000, 0.000000000000000000, 0.000000000000000000 ) ) ;
#4123=CARTESIAN_POINT ( 'NONE',  ( -0.7500000000000000000, -2.749999999999995559, 1.500000000000000000 ) ) ;
#4130=ORIENTED_EDGE ( 'NONE', *, *, #4597, .T. ) ;
#4131=EDGE_CURVE ( 'NONE', #3545, #2406, #6089, .T. ) ;
#4133=APPLICATION_CONTEXT ( 'automotive_design' ) ;
#4137=CARTESIAN_POINT ( 'NONE',  ( 0.000000000000000000, 0.000000000000000000, 21.00000000000000000 ) ) ;
#4179=ORIENTED_EDGE ( 'NONE', *, *, #2848, .T. ) ;
#4193=EDGE_LOOP ( 'NONE', ( #1763, #5432, #3804, #5728 ) ) ;
#4205=DIRECTION ( 'NONE',  ( 1.224646799147353207E-16, 1.000000000000000000, -0.000000000000000000 ) ) ;
#4210=DIRECTION ( 'NONE',  ( 0.000000000000000000, 0.000000000000000000, -1.000000000000000000 ) ) ;
#4216=EDGE_CURVE ( 'NONE', #8987, #7578, #3381, .T. ) ;
#4245=EDGE_CURVE ( 'NONE', #6044, #5505, #4825, .T. ) ;
#4273=LINE ( 'NONE', #2512, #2103 ) ;
#4280=EDGE_LOOP ( 'NONE', ( #1213, #7606, #1879, #5006 ) ) ;
#4292=ORIENTED_EDGE ( 'NONE', *, *, #4245, .T. ) ;
#4331=FACE_OUTER_BOUND ( 'NONE', #5514, .T. ) ;
#4339=VERTEX_POINT ( 'NONE', #7992 ) ;
#4367=DIRECTION ( 'NONE',  ( -0.000000000000000000, 1.000000000000000000, -0.000000000000000000 ) ) ;
#4371=ORIENTED_EDGE ( 'NONE', *, *, #6356, .T. ) ;
#4406=AXIS2_PLACEMENT_3D ( 'NONE', #6445, #4939, #7146 ) ;
#4416=PLANE ( 'NONE',  #6360 ) ;
#4421=ORIENTED_EDGE ( 'NONE', *, *, #1125, .T. ) ;
#4425=ORIENTED_EDGE ( 'NONE', *, *, #8629, .F. ) ;
#4432=CARTESIAN_POINT ( 'NONE',  ( 6.000000000000000888, 7.347880794884120722E-16, 1.000000000000000000 ) ) ;
#4433=AXIS2_PLACEMENT_3D ( 'NONE', #2680, #605, #6428 ) ;
#4442=ADVANCED_FACE ( 'NONE', ( #5880 ), #1503, .T. ) ;
#4455=DIRECTION ( 'NONE',  ( -0.7071067811865507924, -0.7071067811865441310, 0.000000000000000000 ) ) ;
#4460=ORIENTED_EDGE ( 'NONE', *, *, #4131, .T. ) ;
#4468=DIRECTION ( 'NONE',  ( 1.000000000000000000, -0.000000000000000000, -0.000000000000000000 ) ) ;
#4480=FACE_OUTER_BOUND ( 'NONE', #2224, .T. ) ;
#4494=CARTESIAN_POINT ( 'NONE',  ( -0.7500000000000000000, -2.749999999999995559, 1.500000000000000000 ) ) ;
#4503=ORIENTED_EDGE ( 'NONE', *, *, #269, .T. ) ;
#4508=EDGE_LOOP ( 'NONE', ( #2520, #1014, #7003, #2619 ) ) ;
#4514=LINE ( 'NONE', #7441, #2426 ) ;
#4539=DIRECTION ( 'NONE',  ( 1.000000000000000000, 0.000000000000000000, 0.000000000000000000 ) ) ;
#4541=CARTESIAN_POINT ( 'NONE',  ( -0.7500000000000000000, -2.749999999999995559, 1.500000000000000000 ) ) ;
#4542=CARTESIAN_POINT ( 'NONE',  ( 4.119968255444916849E-15, 3.500000000000000000, 1.500000000000000000 ) ) ;
#4554=EDGE_CURVE ( 'NONE', #2584, #4960, #8184, .T. ) ;
#4597=EDGE_CURVE ( 'NONE', #9178, #3545, #1787, .T. ) ;
#4599=DIRECTION ( 'NONE',  ( 0.000000000000000000, -1.000000000000000000, 0.000000000000000000 ) ) ;
#4611=CARTESIAN_POINT ( 'NONE',  ( -6.000000000000000888, 0.000000000000000000, 5.000000000000000000 ) ) ;
#4612=ORIENTED_EDGE ( 'NONE', *, *, #3731, .T. ) ;
#4633=ORIENTED_EDGE ( 'NONE', *, *, #1957, .F. ) ;
#4636=EDGE_CURVE ( 'NONE', #5576, #956, #7659, .T. ) ;
#4665=DIRECTION ( 'NONE',  ( 0.000000000000000000, 0.000000000000000000, -1.000000000000000000 ) ) ;
#4679=LINE ( 'NONE', #2566, #6401 ) ;
#4680=CARTESIAN_POINT ( 'NONE',  ( 0.7500000000000000000, 0.7500000000000000000, 1.500000000000000000 ) ) ;
#4685=EDGE_LOOP ( 'NONE', ( #5224, #764, #4633, #6780, #5599, #3465, #5861, #4959, #2178, #1521, #5813, #5262, #7767, #4130, #6330, #7744 ) ) ;
#4687=DIRECTION ( 'NONE',  ( 1.000000000000000000, 0.000000000000000000, 0.000000000000000000 ) ) ;
#4697=CARTESIAN_POINT ( 'NONE',  ( 0.000000000000000000, 0.000000000000000000, 4.000000000000000000 ) ) ;
#4699=FACE_OUTER_BOUND ( 'NONE', #3987, .T. ) ;
#4713=ADVANCED_FACE ( 'NONE', ( #8321 ), #1742, .F. ) ;
#4731=ADVANCED_FACE ( 'NONE', ( #531 ), #7885, .T. ) ;
#4739=CARTESIAN_POINT ( 'NONE',  ( -0.7500000000000000000, 2.750000000000002665, 0.000000000000000000 ) ) ;
#4748=ORIENTED_EDGE ( 'NONE', *, *, #7365, .T. ) ;
#4757=ORIENTED_EDGE ( 'NONE', *, *, #8346, .T. ) ;
#4761=CONICAL_SURFACE ( 'NONE', #6287, 2.499999999999998668, 0.7853981633974461696 ) ;
#4766=CARTESIAN_POINT ( 'NONE',  ( -0.7500000000000000000, -0.7500000000000000000, 1.500000000000000000 ) ) ;
#4792=VERTEX_POINT ( 'NONE', #5590 ) ;
#4825=LINE ( 'NONE', #6325, #7218 ) ;
#4846=ADVANCED_FACE ( 'NONE', ( #6500 ), #4761, .T. ) ;
#4851=DIRECTION ( 'NONE',  ( 0.000000000000000000, -0.000000000000000000, 1.000000000000000000 ) ) ;
#4854=DIRECTION ( 'NONE',  ( 0.000000000000000000, -0.000000000000000000, -1.000000000000000000 ) ) ;
#4870=CARTESIAN_POINT ( 'NONE',  ( -5.000000000000000888, 6.735557395310443009E-16, 0.000000000000000000 ) ) ;
#4890=AXIS2_PLACEMENT_3D ( 'NONE', #1608, #3866, #4687 ) ;
#4893=ORIENTED_EDGE ( 'NONE', *, *, #1532, .F. ) ;
#4897=AXIS2_PLACEMENT_3D ( 'NONE', #8462, #6787, #1062 ) ;
#4898=PLANE ( 'NONE',  #3443 ) ;
#4921=FACE_OUTER_BOUND ( 'NONE', #408, .T. ) ;
#4931=CARTESIAN_POINT ( 'NONE',  ( 0.000000000000000000, 0.000000000000000000, 20.49999999999999645 ) ) ;
#4939=DIRECTION ( 'NONE',  ( 0.000000000000000000, 0.000000000000000000, 1.000000000000000000 ) ) ;
#4944=DIRECTION ( 'NONE',  ( 0.000000000000000000, 0.000000000000000000, -1.000000000000000000 ) ) ;
#4953=EDGE_CURVE ( 'NONE', #3755, #3545, #5913, .T. ) ;
#4955=CARTESIAN_POINT ( 'NONE',  ( 2.749999999999996447, -0.7500000000000000000, 1.500000000000000000 ) ) ;
#4959=ORIENTED_EDGE ( 'NONE', *, *, #2604, .F. ) ;
#4960=VERTEX_POINT ( 'NONE', #1540 ) ;
#4971=EDGE_LOOP ( 'NONE', ( #482, #9252, #7037, #5645 ) ) ;
#4979=DIRECTION ( 'NONE',  ( 0.7071067811865444641, -0.7071067811865505703, -0.000000000000000000 ) ) ;
#4983=FACE_BOUND ( 'NONE', #989, .T. ) ;
#5006=ORIENTED_EDGE ( 'NONE', *, *, #5463, .T. ) ;
#5019=AXIS2_PLACEMENT_3D ( 'NONE', #5098, #8030, #7355 ) ;
#5054=DIRECTION ( 'NONE',  ( 0.000000000000000000, 0.000000000000000000, 1.000000000000000000 ) ) ;
#5055=CARTESIAN_POINT ( 'NONE',  ( -3.500000000000000000, 4.119968255444916849E-15, 1.500000000000000000 ) ) ;
#5057=CARTESIAN_POINT ( 'NONE',  ( 3.000000000000000444, 3.673940397442060361E-16, 20.49999999999999645 ) ) ;
#5073=AXIS2_PLACEMENT_3D ( 'NONE', #8196, #7327, #7420 ) ;
#5093=DIRECTION ( 'NONE',  ( -0.000000000000000000, 0.000000000000000000, -1.000000000000000000 ) ) ;
#5097=DIRECTION ( 'NONE',  ( 1.000000000000000000, 0.000000000000000000, 0.000000000000000000 ) ) ;
#5098=CARTESIAN_POINT ( 'NONE',  ( 0.000000000000000000, 0.000000000000000000, 21.00000000000000000 ) ) ;
#5103=VECTOR ( 'NONE', #9051, 1000.000000000000000 ) ;
#5108=VERTEX_POINT ( 'NONE', #916 ) ;
#5150=ORIENTED_EDGE ( 'NONE', *, *, #5416, .T. ) ;
#5178=ORIENTED_EDGE ( 'NONE', *, *, #6593, .F. ) ;
#5182=ADVANCED_FACE ( 'NONE', ( #519 ), #1920, .T. ) ;
#5183=VECTOR ( 'NONE', #5226, 1000.000000000000000 ) ;
#5220=CARTESIAN_POINT ( 'NONE',  ( 5.000000000000000888, 0.000000000000000000, 4.000000000000000000 ) ) ;
#5221=LINE ( 'NONE', #8869, #2685 ) ;
#5224=ORIENTED_EDGE ( 'NONE', *, *, #6338, .T. ) ;
#5226=DIRECTION ( 'NONE',  ( -0.000000000000000000, -0.000000000000000000, -1.000000000000000000 ) ) ;
#5237=ADVANCED_FACE ( 'NONE', ( #8773 ), #4898, .F. ) ;
#5240=CARTESIAN_POINT ( 'NONE',  ( 0.7500000000000000000, -0.7500000000000000000, 1.500000000000000000 ) ) ;
#5253=AXIS2_PLACEMENT_3D ( 'NONE', #205, #5821, #4040 ) ;
#5257=VECTOR ( 'NONE', #6025, 1000.000000000000000 ) ;
#5262=ORIENTED_EDGE ( 'NONE', *, *, #8639, .F. ) ;
#5275=CARTESIAN_POINT ( 'NONE',  ( -0.7500000000000000000, 0.7500000000000000000, 0.000000000000000000 ) ) ;
#5283=DIRECTION ( 'NONE',  ( 0.000000000000000000, 1.000000000000000000, 0.000000000000000000 ) ) ;
#5284=UNCERTAINTY_MEASURE_WITH_UNIT (LENGTH_MEASURE( 1.000000000000000082E-05 ), #2436, 'distance_accuracy_value', 'NONE');
#5291=AXIS2_PLACEMENT_3D ( 'NONE', #7267, #6469, #9281 ) ;
#5295=CARTESIAN_POINT ( 'NONE',  ( -0.7500000000000000000, -0.7500000000000000000, 1.500000000000000000 ) ) ;
#5301=ADVANCED_FACE ( 'NONE', ( #6345 ), #1667, .T. ) ;
#5314=CARTESIAN_POINT ( 'NONE',  ( -0.7500000000000000000, -0.7500000000000000000, 0.000000000000000000 ) ) ;
#5330=VECTOR ( 'NONE', #9288, 1000.000000000000000 ) ;
#5342=EDGE_CURVE ( 'NONE', #956, #1434, #2381, .T. ) ;
#5362=ORIENTED_EDGE ( 'NONE', *, *, #2604, .T. ) ;
#5405=ORIENTED_EDGE ( 'NONE', *, *, #4597, .F. ) ;
#5410=FACE_OUTER_BOUND ( 'NONE', #2722, .T. ) ;
#5416=EDGE_CURVE ( 'NONE', #6441, #5921, #3872, .T. ) ;
#5423=EDGE_CURVE ( 'NONE', #3262, #2860, #8511, .T. ) ;
#5430=ORIENTED_EDGE ( 'NONE', *, *, #6530, .T. ) ;
#5432=ORIENTED_EDGE ( 'NONE', *, *, #9144, .T. ) ;
#5433=AXIS2_PLACEMENT_3D ( 'NONE', #6952, #362, #457 ) ;
#5451=ORIENTED_EDGE ( 'NONE', *, *, #6846, .T. ) ;
#5453=ORIENTED_EDGE ( 'NONE', *, *, #8909, .T. ) ;
#5463=EDGE_CURVE ( 'NONE', #6611, #3327, #7429, .T. ) ;
#5491=VECTOR ( 'NONE', #1982, 1000.000000000000000 ) ;
#5501=CIRCLE ( 'NONE', #734, 1.000000000000000000 ) ;
#5504=DIRECTION ( 'NONE',  ( 0.000000000000000000, 0.000000000000000000, 1.000000000000000000 ) ) ;
#5505=VERTEX_POINT ( 'NONE', #7759 ) ;
#5514=EDGE_LOOP ( 'NONE', ( #8648, #5150, #5910, #8942 ) ) ;
#5517=CIRCLE ( 'NONE', #3360, 6.000000000000000888 ) ;
#5524=CARTESIAN_POINT ( 'NONE',  ( -1.750000000000013101, -1.749999999999997780, 0.000000000000000000 ) ) ;
#5546=CARTESIAN_POINT ( 'NONE',  ( 3.500000000000000444, -6.505213034913026604E-16, 1.500000000000000000 ) ) ;
#5563=ORIENTED_EDGE ( 'NONE', *, *, #6593, .T. ) ;
#5567=FACE_OUTER_BOUND ( 'NONE', #5883, .T. ) ;
#5573=VECTOR ( 'NONE', #581, 1000.000000000000000 ) ;
#5576=VERTEX_POINT ( 'NONE', #360 ) ;
#5585=EDGE_LOOP ( 'NONE', ( #8499, #8343, #5831, #1458 ) ) ;
#5590=CARTESIAN_POINT ( 'NONE',  ( 5.000000000000000888, 0.000000000000000000, 0.000000000000000000 ) ) ;
#5599=ORIENTED_EDGE ( 'NONE', *, *, #1532, .T. ) ;
#5613=EDGE_LOOP ( 'NONE', ( #5621, #4503, #4893, #6319 ) ) ;
#5621=ORIENTED_EDGE ( 'NONE', *, *, #3128, .F. ) ;
#5636=DIRECTION ( 'NONE',  ( -0.000000000000000000, -0.000000000000000000, -1.000000000000000000 ) ) ;
#5641=AXIS2_PLACEMENT_3D ( 'NONE', #8182, #7264, #2275 ) ;
#5645=ORIENTED_EDGE ( 'NONE', *, *, #9181, .F. ) ;
#5654=CARTESIAN_POINT ( 'NONE',  ( 2.499999999999998668, 3.367778697655220519E-16, 21.00000000000000000 ) ) ;
#5676=ADVANCED_FACE ( 'NONE', ( #6560 ), #2082, .F. ) ;
#5687=CARTESIAN_POINT ( 'NONE',  ( -2.749999999999995559, 0.7500000000000000000, 1.500000000000000000 ) ) ;
#5707=CARTESIAN_POINT ( 'NONE',  ( -6.000000000000000888, 0.000000000000000000, 1.000000000000000000 ) ) ;
#5728=ORIENTED_EDGE ( 'NONE', *, *, #9402, .F. ) ;
#5731=CARTESIAN_POINT ( 'NONE',  ( -4.119968255444916849E-15, -3.500000000000000000, 1.500000000000000000 ) ) ;
#5739=AXIS2_PLACEMENT_3D ( 'NONE', #6240, #9106, #6152 ) ;
#5744=VECTOR ( 'NONE', #1711, 1000.000000000000000 ) ;
#5766=CARTESIAN_POINT ( 'NONE',  ( 3.000000000000000444, 3.673940397442060361E-16, 5.000000000000000000 ) ) ;
#5768=DIRECTION ( 'NONE',  ( 0.000000000000000000, -1.000000000000000000, 0.000000000000000000 ) ) ;
#5770=ORIENTED_EDGE ( 'NONE', *, *, #8737, .T. ) ;
#5795=ORIENTED_EDGE ( 'NONE', *, *, #9399, .T. ) ;
#5805=ORIENTED_EDGE ( 'NONE', *, *, #8006, .T. ) ;
#5806=FACE_OUTER_BOUND ( 'NONE', #4971, .T. ) ;
#5813=ORIENTED_EDGE ( 'NONE', *, *, #2127, .F. ) ;
#5821=DIRECTION ( 'NONE',  ( 0.000000000000000000, 0.000000000000000000, 1.000000000000000000 ) ) ;
#5831=ORIENTED_EDGE ( 'NONE', *, *, #6846, .F. ) ;
#5838=VERTEX_POINT ( 'NONE', #880 ) ;
#5852=ORIENTED_EDGE ( 'NONE', *, *, #1335, .T. ) ;
#5861=ORIENTED_EDGE ( 'NONE', *, *, #7954, .F. ) ;
#5880=FACE_OUTER_BOUND ( 'NONE', #4280, .T. ) ;
#5883=EDGE_LOOP ( 'NONE', ( #5178, #2170, #3420, #8963 ) ) ;
#5898=DIRECTION ( 'NONE',  ( 0.000000000000000000, 0.000000000000000000, -1.000000000000000000 ) ) ;
#5910=ORIENTED_EDGE ( 'NONE', *, *, #6963, .F. ) ;
#5913=LINE ( 'NONE', #2265, #8445 ) ;
#5921=VERTEX_POINT ( 'NONE', #9086 ) ;
#5958=VERTEX_POINT ( 'NONE', #5546 ) ;
#5959=ORIENTED_EDGE ( 'NONE', *, *, #1663, .F. ) ;
#5965=CIRCLE ( 'NONE', #6582, 3.000000000000000444 ) ;
#5976=( NAMED_UNIT ( * ) SI_UNIT ( $, .STERADIAN. ) SOLID_ANGLE_UNIT ( ) );
#6005=CARTESIAN_POINT ( 'NONE',  ( -0.7500000000000000000, -0.7500000000000000000, 0.000000000000000000 ) ) ;
#6025=DIRECTION ( 'NONE',  ( 0.000000000000000000, 0.000000000000000000, -1.000000000000000000 ) ) ;
#6032=ORIENTED_EDGE ( 'NONE', *, *, #2518, .T. ) ;
#6044=VERTEX_POINT ( 'NONE', #4955 ) ;
#6049=LINE ( 'NONE', #796, #2742 ) ;
#6054=VECTOR ( 'NONE', #4367, 1000.000000000000000 ) ;
#6064=AXIS2_PLACEMENT_3D ( 'NONE', #3775, #6715, #132 ) ;
#6069=PRODUCT_DEFINITION ( 'UNKNOWN', '', #8063, #8925 ) ;
#6088=CYLINDRICAL_SURFACE ( 'NONE', #7307, 3.000000000000000444 ) ;
#6089=LINE ( 'NONE', #3681, #6162 ) ;
#6126=LINE ( 'NONE', #2474, #411 ) ;
#6141=CARTESIAN_POINT ( 'NONE',  ( 0.7500000000000000000, -0.7500000000000000000, 1.500000000000000000 ) ) ;
#6142=LINE ( 'NONE', #7564, #4091 ) ;
#6149=FACE_OUTER_BOUND ( 'NONE', #2591, .T. ) ;
#6150=ORIENTED_EDGE ( 'NONE', *, *, #1836, .F. ) ;
#6152=DIRECTION ( 'NONE',  ( -1.000000000000000000, 0.000000000000000000, 0.000000000000000000 ) ) ;
#6155=LINE ( 'NONE', #372, #8150 ) ;
#6162=VECTOR ( 'NONE', #6618, 1000.000000000000000 ) ;
#6163=LINE ( 'NONE', #2363, #8556 ) ;
#6165=CARTESIAN_POINT ( 'NONE',  ( 1.750000000000001554, 1.749999999999984235, 0.000000000000000000 ) ) ;
#6172=LINE ( 'NONE', #9082, #1878 ) ;
#6182=( NAMED_UNIT ( * ) PLANE_ANGLE_UNIT ( ) SI_UNIT ( $, .RADIAN. ) );
#6198=CARTESIAN_POINT ( 'NONE',  ( 2.749999999999996447, -0.7500000000000000000, 0.000000000000000000 ) ) ;
#6211=VECTOR ( 'NONE', #2642, 1000.000000000000000 ) ;
#6214=DIRECTION ( 'NONE',  ( 0.000000000000000000, 0.000000000000000000, 1.000000000000000000 ) ) ;
#6240=CARTESIAN_POINT ( 'NONE',  ( 0.000000000000000000, 0.000000000000000000, 5.000000000000000000 ) ) ;
#6247=CARTESIAN_POINT ( 'NONE',  ( 0.7500000000000000000, -0.7500000000000000000, 0.000000000000000000 ) ) ;
#6253=ORIENTED_EDGE ( 'NONE', *, *, #3731, .F. ) ;
#6259=EDGE_CURVE ( 'NONE', #6631, #2159, #9384, .T. ) ;
#6272=CIRCLE ( 'NONE', #1336, 5.000000000000000888 ) ;
#6276=CARTESIAN_POINT ( 'NONE',  ( 1.750000000000015987, 1.749999999999999778, 0.000000000000000000 ) ) ;
#6285=TOROIDAL_SURFACE ( 'NONE', #4433, 5.000000000000000888, 1.000000000000000000 ) ;
#6286=CARTESIAN_POINT ( 'NONE',  ( -1.750000000000001554, -1.749999999999984235, 0.000000000000000000 ) ) ;
#6287=AXIS2_PLACEMENT_3D ( 'NONE', #6597, #7301, #6683 ) ;
#6308=FACE_OUTER_BOUND ( 'NONE', #8517, .T. ) ;
#6319=ORIENTED_EDGE ( 'NONE', *, *, #9144, .F. ) ;
#6325=CARTESIAN_POINT ( 'NONE',  ( 0.7500000000000000000, -0.7500000000000000000, 1.500000000000000000 ) ) ;
#6330=ORIENTED_EDGE ( 'NONE', *, *, #4953, .F. ) ;
#6335=DIRECTION ( 'NONE',  ( 0.7071067811865505703, 0.7071067811865444641, -0.000000000000000000 ) ) ;
#6338=EDGE_CURVE ( 'NONE', #7970, #2895, #3997, .T. ) ;
#6345=FACE_OUTER_BOUND ( 'NONE', #1597, .T. ) ;
#6347=DIRECTION ( 'NONE',  ( 1.000000000000000000, 0.000000000000000000, -0.000000000000000000 ) ) ;
#6356=EDGE_CURVE ( 'NONE', #991, #2334, #6049, .T. ) ;
#6360=AXIS2_PLACEMENT_3D ( 'NONE', #760, #5283, #8828 ) ;
#6362=VERTEX_POINT ( 'NONE', #2297 ) ;
#6363=ORIENTED_EDGE ( 'NONE', *, *, #6943, .T. ) ;
#6366=EDGE_CURVE ( 'NONE', #956, #3327, #1621, .T. ) ;
#6370=VECTOR ( 'NONE', #3634, 999.9999999999998863 ) ;
#6385=( GEOMETRIC_REPRESENTATION_CONTEXT ( 3 ) GLOBAL_UNCERTAINTY_ASSIGNED_CONTEXT ( ( #5284 ) ) GLOBAL_UNIT_ASSIGNED_CONTEXT ( ( #2436, #6182, #9090 ) ) REPRESENTATION_CONTEXT ( 'NONE', 'WORKASPACE' ) );
#6401=VECTOR ( 'NONE', #7599, 1000.000000000000000 ) ;
#6409=DIRECTION ( 'NONE',  ( -0.000000000000000000, -0.000000000000000000, -1.000000000000000000 ) ) ;
#6427=VERTEX_POINT ( 'NONE', #9107 ) ;
#6428=DIRECTION ( 'NONE',  ( 1.000000000000000000, 0.000000000000000000, 0.000000000000000000 ) ) ;
#6440=VECTOR ( 'NONE', #3231, 1000.000000000000114 ) ;
#6441=VERTEX_POINT ( 'NONE', #8492 ) ;
#6445=CARTESIAN_POINT ( 'NONE',  ( 0.000000000000000000, 0.000000000000000000, 1.000000000000000000 ) ) ;
#6462=LINE ( 'NONE', #776, #8693 ) ;
#6469=DIRECTION ( 'NONE',  ( 0.000000000000000000, 1.000000000000000000, -0.000000000000000000 ) ) ;
#6487=DIRECTION ( 'NONE',  ( 0.000000000000000000, 0.000000000000000000, -1.000000000000000000 ) ) ;
#6491=CARTESIAN_POINT ( 'NONE',  ( 0.000000000000000000, 0.000000000000000000, 21.00000000000000000 ) ) ;
#6500=FACE_OUTER_BOUND ( 'NONE', #2724, .T. ) ;
#6503=PLANE ( 'NONE',  #273 ) ;
#6514=ORIENTED_EDGE ( 'NONE', *, *, #4953, .T. ) ;
#6530=EDGE_CURVE ( 'NONE', #3262, #3430, #7001, .T. ) ;
#6555=ORIENTED_EDGE ( 'NONE', *, *, #3550, .F. ) ;
#6560=FACE_OUTER_BOUND ( 'NONE', #4193, .T. ) ;
#6566=MECHANICAL_DESIGN_GEOMETRIC_PRESENTATION_REPRESENTATION('',(#8089),#2726);
#6582=AXIS2_PLACEMENT_3D ( 'NONE', #2338, #8905, #2909 ) ;
#6591=VECTOR ( 'NONE', #2268, 1000.000000000000000 ) ;
#6593=EDGE_CURVE ( 'NONE', #5576, #2697, #5501, .T. ) ;
#6597=CARTESIAN_POINT ( 'NONE',  ( 0.000000000000000000, 0.000000000000000000, 21.00000000000000000 ) ) ;
#6611=VERTEX_POINT ( 'NONE', #5707 ) ;
#6618=DIRECTION ( 'NONE',  ( 0.000000000000000000, 0.000000000000000000, 1.000000000000000000 ) ) ;
#6631=VERTEX_POINT ( 'NONE', #7228 ) ;
#6636=ORIENTED_EDGE ( 'NONE', *, *, #9402, .T. ) ;
#6642=DIRECTION ( 'NONE',  ( 0.000000000000000000, 0.000000000000000000, 1.000000000000000000 ) ) ;
#6655=ORIENTED_EDGE ( 'NONE', *, *, #950, .F. ) ;
#6673=AXIS2_PLACEMENT_3D ( 'NONE', #4494, #3729, #6806 ) ;
#6677=CARTESIAN_POINT ( 'NONE',  ( 0.7500000000000000000, 2.749999999999995559, 1.500000000000000000 ) ) ;
#6683=DIRECTION ( 'NONE',  ( -1.000000000000000000, 0.000000000000000000, 0.000000000000000000 ) ) ;
#6692=AXIS2_PLACEMENT_3D ( 'NONE', #4074, #3891, #9200 ) ;
#6711=EDGE_CURVE ( 'NONE', #4960, #2537, #2953, .T. ) ;
#6715=DIRECTION ( 'NONE',  ( 0.000000000000000000, 0.000000000000000000, 1.000000000000000000 ) ) ;
#6725=ORIENTED_EDGE ( 'NONE', *, *, #1806, .F. ) ;
#6760=CARTESIAN_POINT ( 'NONE',  ( 0.000000000000000000, 0.000000000000000000, 0.000000000000000000 ) ) ;
#6780=ORIENTED_EDGE ( 'NONE', *, *, #2919, .F. ) ;
#6787=DIRECTION ( 'NONE',  ( 0.000000000000000000, 0.000000000000000000, 1.000000000000000000 ) ) ;
#6790=( NAMED_UNIT ( * ) PLANE_ANGLE_UNIT ( ) SI_UNIT ( $, .RADIAN. ) );
#6793=CARTESIAN_POINT ( 'NONE',  ( -0.7500000000000000000, -2.749999999999995559, 0.000000000000000000 ) ) ;
#6806=DIRECTION ( 'NONE',  ( 0.000000000000000000, 0.000000000000000000, 1.000000000000000000 ) ) ;
#6846=EDGE_CURVE ( 'NONE', #8186, #4960, #7517, .T. ) ;
#6860=VERTEX_POINT ( 'NONE', #5314 ) ;
#6893=DIRECTION ( 'NONE',  ( 0.000000000000000000, 0.000000000000000000, -1.000000000000000000 ) ) ;
#6898=ORIENTED_EDGE ( 'NONE', *, *, #8993, .F. ) ;
#6939=EDGE_LOOP ( 'NONE', ( #2853, #514, #1580, #8805 ) ) ;
#6943=EDGE_CURVE ( 'NONE', #8301, #6611, #9238, .T. ) ;
#6951=AXIS2_PLACEMENT_3D ( 'NONE', #7506, #7653, #167 ) ;
#6952=CARTESIAN_POINT ( 'NONE',  ( 2.749999999999996447, -0.7500000000000000000, 1.500000000000000000 ) ) ;
#6963=EDGE_CURVE ( 'NONE', #5505, #5921, #1077, .T. ) ;
#6972=CARTESIAN_POINT ( 'NONE',  ( -2.499999999999998668, 0.000000000000000000, 21.00000000000000000 ) ) ;
#6990=CARTESIAN_POINT ( 'NONE',  ( 0.000000000000000000, 0.000000000000000000, 21.00000000000000000 ) ) ;
#6994=PLANE ( 'NONE',  #5433 ) ;
#7001=LINE ( 'NONE', #1765, #8866 ) ;
#7003=ORIENTED_EDGE ( 'NONE', *, *, #6338, .F. ) ;
#7015=DIRECTION ( 'NONE',  ( -0.7071067811865460184, 0.000000000000000000, -0.7071067811865489050 ) ) ;
#7023=EDGE_LOOP ( 'NONE', ( #6514, #4460, #3911, #5453 ) ) ;
#7024=CIRCLE ( 'NONE', #1800, 5.000000000000000888 ) ;
#7028=DIRECTION ( 'NONE',  ( 1.000000000000000000, 0.000000000000000000, 0.000000000000000000 ) ) ;
#7037=ORIENTED_EDGE ( 'NONE', *, *, #2848, .F. ) ;
#7045=DIRECTION ( 'NONE',  ( 0.000000000000000000, 0.000000000000000000, -1.000000000000000000 ) ) ;
#7048=DIRECTION ( 'NONE',  ( -0.000000000000000000, -1.000000000000000000, -0.000000000000000000 ) ) ;
#7056=LINE ( 'NONE', #7909, #6211 ) ;
#7057=LINE ( 'NONE', #5524, #8095 ) ;
#7091=LINE ( 'NONE', #654, #2405 ) ;
#7117=LINE ( 'NONE', #538, #2416 ) ;
#7128=LINE ( 'NONE', #7761, #664 ) ;
#7142=ORIENTED_EDGE ( 'NONE', *, *, #6366, .T. ) ;
#7146=DIRECTION ( 'NONE',  ( 1.000000000000000000, 0.000000000000000000, 0.000000000000000000 ) ) ;
#7150=CARTESIAN_POINT ( 'NONE',  ( -0.7500000000000000000, 0.7500000000000000000, 1.500000000000000000 ) ) ;
#7156=ORIENTED_EDGE ( 'NONE', *, *, #3828, .F. ) ;
#7159=CARTESIAN_POINT ( 'NONE',  ( -3.500000000000000000, 4.119968255444916849E-15, 1.500000000000000000 ) ) ;
#7172=VECTOR ( 'NONE', #430, 1000.000000000000000 ) ;
#7198=DIRECTION ( 'NONE',  ( 1.000000000000000000, 0.000000000000000000, 0.000000000000000000 ) ) ;
#7205=ORIENTED_EDGE ( 'NONE', *, *, #7365, .F. ) ;
#7217=DIRECTION ( 'NONE',  ( -0.000000000000000000, -0.000000000000000000, -1.000000000000000000 ) ) ;
#7218=VECTOR ( 'NONE', #1754, 1000.000000000000000 ) ;
#7228=CARTESIAN_POINT ( 'NONE',  ( -2.499999999999998668, 0.000000000000000000, 21.00000000000000000 ) ) ;
#7245=ADVANCED_FACE ( 'NONE', ( #8138, #4480 ), #639, .F. ) ;
#7264=DIRECTION ( 'NONE',  ( 0.7071067811865444641, -0.7071067811865505703, -0.000000000000000000 ) ) ;
#7267=CARTESIAN_POINT ( 'NONE',  ( -0.7500000000000000000, 0.7500000000000000000, 1.500000000000000000 ) ) ;
#7277=AXIS2_PLACEMENT_3D ( 'NONE', #7567, #1709, #7471 ) ;
#7286=DIRECTION ( 'NONE',  ( -0.000000000000000000, 1.000000000000000000, -0.000000000000000000 ) ) ;
#7289=ADVANCED_FACE ( 'NONE', ( #2565 ), #7553, .F. ) ;
#7301=DIRECTION ( 'NONE',  ( 0.000000000000000000, 0.000000000000000000, -1.000000000000000000 ) ) ;
#7307=AXIS2_PLACEMENT_3D ( 'NONE', #6990, #3198, #9003 ) ;
#7323=EDGE_CURVE ( 'NONE', #991, #8987, #970, .T. ) ;
#7327=DIRECTION ( 'NONE',  ( 0.000000000000000000, 0.000000000000000000, 1.000000000000000000 ) ) ;
#7337=AXIS2_PLACEMENT_3D ( 'NONE', #7623, #1044, #3984 ) ;
#7349=CARTESIAN_POINT ( 'NONE',  ( -0.7500000000000000000, 0.7500000000000000000, 1.500000000000000000 ) ) ;
#7355=DIRECTION ( 'NONE',  ( -1.000000000000000000, 0.000000000000000000, 0.000000000000000000 ) ) ;
#7365=EDGE_CURVE ( 'NONE', #763, #7578, #6172, .T. ) ;
#7371=DIRECTION ( 'NONE',  ( 0.7071067811865505703, 0.7071067811865444641, -0.000000000000000000 ) ) ;
#7380=DIRECTION ( 'NONE',  ( 0.000000000000000000, 0.000000000000000000, 1.000000000000000000 ) ) ;
#7384=PRODUCT ( '6-M6-16', '6-M6-16', '', ( #244 ) ) ;
#7420=DIRECTION ( 'NONE',  ( 1.000000000000000000, 0.000000000000000000, 0.000000000000000000 ) ) ;
#7427=ORIENTED_EDGE ( 'NONE', *, *, #5463, .F. ) ;
#7429=CIRCLE ( 'NONE', #6064, 6.000000000000000888 ) ;
#7434=CARTESIAN_POINT ( 'NONE',  ( -5.000000000000000888, 6.735557395310443009E-16, 5.000000000000000000 ) ) ;
#7435=DIRECTION ( 'NONE',  ( -0.7071067811865510144, -0.7071067811865441310, 0.000000000000000000 ) ) ;
#7441=CARTESIAN_POINT ( 'NONE',  ( -2.750000000000002665, -0.7500000000000000000, 1.500000000000000000 ) ) ;
#7471=DIRECTION ( 'NONE',  ( 1.000000000000000000, 0.000000000000000000, 0.000000000000000000 ) ) ;
#7479=DIRECTION ( 'NONE',  ( 1.000000000000000000, 0.000000000000000000, -0.000000000000000000 ) ) ;
#7486=UNCERTAINTY_MEASURE_WITH_UNIT (LENGTH_MEASURE( 1.000000000000000082E-05 ), #3038, 'distance_accuracy_value', 'NONE');
#7505=EDGE_LOOP ( 'NONE', ( #229, #1619, #3625, #6725 ) ) ;
#7506=CARTESIAN_POINT ( 'NONE',  ( -0.7500000000000000000, -0.7500000000000000000, 1.500000000000000000 ) ) ;
#7515=EDGE_CURVE ( 'NONE', #5921, #763, #1882, .T. ) ;
#7517=LINE ( 'NONE', #8240, #3045 ) ;
#7534=ADVANCED_FACE ( 'NONE', ( #7793 ), #2658, .F. ) ;
#7553=PLANE ( 'NONE',  #6951 ) ;
#7556=CARTESIAN_POINT ( 'NONE',  ( 0.000000000000000000, 0.000000000000000000, 4.000000000000000000 ) ) ;
#7564=CARTESIAN_POINT ( 'NONE',  ( 1.749999999999985345, -1.750000000000001554, 0.000000000000000000 ) ) ;
#7567=CARTESIAN_POINT ( 'NONE',  ( 0.000000000000000000, 0.000000000000000000, 20.49999999999999645 ) ) ;
#7576=PLANE ( 'NONE',  #7337 ) ;
#7578=VERTEX_POINT ( 'NONE', #7980 ) ;
#7594=EDGE_CURVE ( 'NONE', #8767, #2584, #3747, .T. ) ;
#7599=DIRECTION ( 'NONE',  ( -1.000000000000000000, -0.000000000000000000, -0.000000000000000000 ) ) ;
#7605=CIRCLE ( 'NONE', #6692, 5.000000000000000888 ) ;
#7606=ORIENTED_EDGE ( 'NONE', *, *, #8695, .T. ) ;
#7623=CARTESIAN_POINT ( 'NONE',  ( -4.119968255444916849E-15, -3.500000000000000000, 1.500000000000000000 ) ) ;
#7627=DIRECTION ( 'NONE',  ( -0.7071067811865441310, 0.7071067811865510144, -0.000000000000000000 ) ) ;
#7628=CIRCLE ( 'NONE', #2875, 1.000000000000000000 ) ;
#7635=VECTOR ( 'NONE', #4455, 1000.000000000000114 ) ;
#7646=ADVANCED_FACE ( 'NONE', ( #8128 ), #2261, .T. ) ;
#7653=DIRECTION ( 'NONE',  ( -1.000000000000000000, 0.000000000000000000, 0.000000000000000000 ) ) ;
#7659=CIRCLE ( 'NONE', #3507, 6.000000000000000888 ) ;
#7660=ORIENTED_EDGE ( 'NONE', *, *, #8140, .F. ) ;
#7695=EDGE_LOOP ( 'NONE', ( #4179, #5430, #1105, #9128 ) ) ;
#7702=EDGE_CURVE ( 'NONE', #1434, #2697, #7605, .T. ) ;
#7735=VECTOR ( 'NONE', #2675, 1000.000000000000000 ) ;
#7744=ORIENTED_EDGE ( 'NONE', *, *, #9399, .F. ) ;
#7753=EDGE_LOOP ( 'NONE', ( #320, #784, #5852, #7427 ) ) ;
#7759=CARTESIAN_POINT ( 'NONE',  ( 0.7500000000000000000, -0.7500000000000000000, 1.500000000000000000 ) ) ;
#7761=CARTESIAN_POINT ( 'NONE',  ( 4.119968255444916849E-15, 3.500000000000000000, 0.000000000000000000 ) ) ;
#7767=ORIENTED_EDGE ( 'NONE', *, *, #8140, .T. ) ;
#7780=LINE ( 'NONE', #1096, #7172 ) ;
#7782=CARTESIAN_POINT ( 'NONE',  ( 0.000000000000000000, 0.000000000000000000, 1.500000000000000000 ) ) ;
#7785=PLANE ( 'NONE',  #3946 ) ;
#7793=FACE_OUTER_BOUND ( 'NONE', #6939, .T. ) ;
#7807=AXIS2_PLACEMENT_3D ( 'NONE', #780, #3672, #1453 ) ;
#7810=EDGE_CURVE ( 'NONE', #2280, #7970, #8309, .T. ) ;
#7830=CARTESIAN_POINT ( 'NONE',  ( 4.119968255444916849E-15, 3.500000000000000000, 1.500000000000000000 ) ) ;
#7833=ORIENTED_EDGE ( 'NONE', *, *, #4636, .T. ) ;
#7841=PRODUCT_DEFINITION_SHAPE ( 'NONE', 'NONE',  #6069 ) ;
#7864=EDGE_CURVE ( 'NONE', #7578, #6441, #7091, .T. ) ;
#7877=ORIENTED_EDGE ( 'NONE', *, *, #3127, .T. ) ;
#7885=PLANE ( 'NONE',  #610 ) ;
#7902=ORIENTED_EDGE ( 'NONE', *, *, #5342, .F. ) ;
#7909=CARTESIAN_POINT ( 'NONE',  ( -0.7500000000000000000, 0.7500000000000000000, 0.000000000000000000 ) ) ;
#7921=FACE_OUTER_BOUND ( 'NONE', #1702, .T. ) ;
#7934=VECTOR ( 'NONE', #3700, 1000.000000000000000 ) ;
#7938=VECTOR ( 'NONE', #7627, 999.9999999999998863 ) ;
#7948=TOROIDAL_SURFACE ( 'NONE', #3801, 5.000000000000000888, 1.000000000000000000 ) ;
#7954=EDGE_CURVE ( 'NONE', #6860, #9262, #8538, .T. ) ;
#7960=CARTESIAN_POINT ( 'NONE',  ( -5.000000000000000888, 6.123233995736767268E-16, 4.000000000000000000 ) ) ;
#7970=VERTEX_POINT ( 'NONE', #38 ) ;
#7980=CARTESIAN_POINT ( 'NONE',  ( -2.818925648462311528E-15, -3.500000000000000000, 0.000000000000000000 ) ) ;
#7981=PLANE ( 'NONE',  #3480 ) ;
#7982=DIRECTION ( 'NONE',  ( 0.7071067811865505703, 0.7071067811865444641, -0.000000000000000000 ) ) ;
#7988=ORIENTED_EDGE ( 'NONE', *, *, #15, .F. ) ;
#7992=CARTESIAN_POINT ( 'NONE',  ( -2.749999999999995559, 0.7500000000000000000, 0.000000000000000000 ) ) ;
#8006=EDGE_CURVE ( 'NONE', #8784, #2406, #178, .T. ) ;
#8012=PLANE ( 'NONE',  #417 ) ;
#8014=CARTESIAN_POINT ( 'NONE',  ( 3.500000000000000444, -6.505213034913026604E-16, 1.500000000000000000 ) ) ;
#8030=DIRECTION ( 'NONE',  ( -0.000000000000000000, -0.000000000000000000, -1.000000000000000000 ) ) ;
#8048=AXIS2_PLACEMENT_3D ( 'NONE', #2913, #9211, #4851 ) ;
#8053=DIRECTION ( 'NONE',  ( -1.000000000000000000, 0.000000000000000000, 0.000000000000000000 ) ) ;
#8063=PRODUCT_DEFINITION_FORMATION_WITH_SPECIFIED_SOURCE ( 'ANY', '', #7384, .NOT_KNOWN. ) ;
#8066=FACE_OUTER_BOUND ( 'NONE', #7023, .T. ) ;
#8089=STYLED_ITEM('',(#9515),#171);
#8095=VECTOR ( 'NONE', #4979, 1000.000000000000000 ) ;
#8112=CARTESIAN_POINT ( 'NONE',  ( 0.000000000000000000, 0.000000000000000000, 5.000000000000000000 ) ) ;
#8128=FACE_OUTER_BOUND ( 'NONE', #5613, .T. ) ;
#8133=CARTESIAN_POINT ( 'NONE',  ( -2.750000000000002665, -0.7500000000000000000, 1.500000000000000000 ) ) ;
#8138=FACE_BOUND ( 'NONE', #4685, .T. ) ;
#8140=EDGE_CURVE ( 'NONE', #3779, #9178, #6142, .T. ) ;
#8150=VECTOR ( 'NONE', #2500, 1000.000000000000114 ) ;
#8155=ADVANCED_FACE ( 'NONE', ( #5410 ), #6088, .T. ) ;
#8182=CARTESIAN_POINT ( 'NONE',  ( 4.119968255444916849E-15, 3.500000000000000000, 1.500000000000000000 ) ) ;
#8184=LINE ( 'NONE', #1600, #3985 ) ;
#8186=VERTEX_POINT ( 'NONE', #4739 ) ;
#8196=CARTESIAN_POINT ( 'NONE',  ( 0.000000000000000000, 0.000000000000000000, 5.000000000000000000 ) ) ;
#8224=EDGE_LOOP ( 'NONE', ( #4425, #6555, #2928, #5405 ) ) ;
#8240=CARTESIAN_POINT ( 'NONE',  ( -0.7500000000000000000, 2.750000000000002665, 1.500000000000000000 ) ) ;
#8253=ORIENTED_EDGE ( 'NONE', *, *, #6963, .T. ) ;
#8265=ORIENTED_EDGE ( 'NONE', *, *, #8993, .T. ) ;
#8282=EDGE_LOOP ( 'NONE', ( #6655, #6363, #1040, #9241 ) ) ;
#8293=CARTESIAN_POINT ( 'NONE',  ( -1.749999999999997780, 1.750000000000013101, 0.000000000000000000 ) ) ;
#8301=VERTEX_POINT ( 'NONE', #4870 ) ;
#8308=ORIENTED_EDGE ( 'NONE', *, *, #7810, .T. ) ;
#8309=LINE ( 'NONE', #1730, #3935 ) ;
#8321=FACE_OUTER_BOUND ( 'NONE', #8378, .T. ) ;
#8324=ORIENTED_EDGE ( 'NONE', *, *, #7702, .F. ) ;
#8331=DIRECTION ( 'NONE',  ( 1.224646799147353207E-16, 1.000000000000000000, -0.000000000000000000 ) ) ;
#8343=ORIENTED_EDGE ( 'NONE', *, *, #6711, .F. ) ;
#8346=EDGE_CURVE ( 'NONE', #2860, #5108, #1215, .T. ) ;
#8378=EDGE_LOOP ( 'NONE', ( #6898, #8308, #5795, #3639 ) ) ;
#8409=ADVANCED_FACE ( 'NONE', ( #8848 ), #1403, .T. ) ;
#8430=AXIS2_PLACEMENT_3D ( 'NONE', #1012, #2414, #9078 ) ;
#8445=VECTOR ( 'NONE', #3080, 1000.000000000000000 ) ;
#8456=ORIENTED_EDGE ( 'NONE', *, *, #7515, .F. ) ;
#8462=CARTESIAN_POINT ( 'NONE',  ( 0.000000000000000000, 0.000000000000000000, 1.000000000000000000 ) ) ;
#8486=CARTESIAN_POINT ( 'NONE',  ( 0.7500000000000000000, -0.7500000000000000000, 0.000000000000000000 ) ) ;
#8489=LINE ( 'NONE', #1998, #5330 ) ;
#8492=CARTESIAN_POINT ( 'NONE',  ( 0.7500000000000000000, -2.750000000000002665, 0.000000000000000000 ) ) ;
#8499=ORIENTED_EDGE ( 'NONE', *, *, #2234, .F. ) ;
#8501=SHAPE_REPRESENTATION ( '6-M6-16', ( #1614 ), #6385 ) ;
#8510=CARTESIAN_POINT ( 'NONE',  ( -0.7500000000000000000, -0.7500000000000000000, 1.500000000000000000 ) ) ;
#8511=CIRCLE ( 'NONE', #7277, 3.000000000000000444 ) ;
#8517=EDGE_LOOP ( 'NONE', ( #9264, #2455, #806, #7988 ) ) ;
#8534=LINE ( 'NONE', #1367, #8976 ) ;
#8538=LINE ( 'NONE', #2682, #263 ) ;
#8556=VECTOR ( 'NONE', #9029, 1000.000000000000000 ) ;
#8564=DIRECTION ( 'NONE',  ( 0.000000000000000000, 0.000000000000000000, 1.000000000000000000 ) ) ;
#8629=EDGE_CURVE ( 'NONE', #5958, #9178, #6126, .T. ) ;
#8636=CIRCLE ( 'NONE', #9094, 2.499999999999998668 ) ;
#8639=EDGE_CURVE ( 'NONE', #3779, #2772, #4679, .T. ) ;
#8648=ORIENTED_EDGE ( 'NONE', *, *, #2127, .T. ) ;
#8657=FACE_OUTER_BOUND ( 'NONE', #2645, .T. ) ;
#8669=ORIENTED_EDGE ( 'NONE', *, *, #950, .T. ) ;
#8683=VECTOR ( 'NONE', #4468, 1000.000000000000000 ) ;
#8693=VECTOR ( 'NONE', #20, 1000.000000000000000 ) ;
#8695=EDGE_CURVE ( 'NONE', #956, #5576, #3487, .T. ) ;
#8715=EDGE_CURVE ( 'NONE', #3397, #6362, #9267, .T. ) ;
#8734=ORIENTED_EDGE ( 'NONE', *, *, #3128, .T. ) ;
#8735=CARTESIAN_POINT ( 'NONE',  ( 0.000000000000000000, 0.000000000000000000, 21.00000000000000000 ) ) ;
#8736=CARTESIAN_POINT ( 'NONE',  ( 2.750000000000006661, 0.7500000000000000000, 0.000000000000000000 ) ) ;
#8737=EDGE_CURVE ( 'NONE', #2697, #1434, #7024, .T. ) ;
#8750=CYLINDRICAL_SURFACE ( 'NONE', #5019, 3.000000000000000444 ) ;
#8767=VERTEX_POINT ( 'NONE', #5687 ) ;
#8773=FACE_OUTER_BOUND ( 'NONE', #3479, .T. ) ;
#8778=DIRECTION ( 'NONE',  ( -1.000000000000000000, 0.000000000000000000, 0.000000000000000000 ) ) ;
#8784=VERTEX_POINT ( 'NONE', #2071 ) ;
#8790=LINE ( 'NONE', #768, #7934 ) ;
#8805=ORIENTED_EDGE ( 'NONE', *, *, #1121, .T. ) ;
#8828=DIRECTION ( 'NONE',  ( 0.000000000000000000, -0.000000000000000000, 1.000000000000000000 ) ) ;
#8848=FACE_OUTER_BOUND ( 'NONE', #5585, .T. ) ;
#8857=VECTOR ( 'NONE', #3118, 1000.000000000000000 ) ;
#8858=ADVANCED_FACE ( 'NONE', ( #4331 ), #7981, .F. ) ;
#8861=AXIS2_PLACEMENT_3D ( 'NONE', #8735, #5898, #8778 ) ;
#8866=VECTOR ( 'NONE', #327, 1000.000000000000000 ) ;
#8868=CARTESIAN_POINT ( 'NONE',  ( 0.7500000000000000000, -2.750000000000002665, 1.500000000000000000 ) ) ;
#8869=CARTESIAN_POINT ( 'NONE',  ( -0.7500000000000000000, -0.7500000000000000000, 1.500000000000000000 ) ) ;
#8905=DIRECTION ( 'NONE',  ( 0.000000000000000000, 0.000000000000000000, 1.000000000000000000 ) ) ;
#8909=EDGE_CURVE ( 'NONE', #8784, #3755, #8790, .T. ) ;
#8925=PRODUCT_DEFINITION_CONTEXT ( 'detailed design', #203, 'design' ) ;
#8942=ORIENTED_EDGE ( 'NONE', *, *, #15, .T. ) ;
#8952=EDGE_CURVE ( 'NONE', #9262, #3397, #4514, .T. ) ;
#8961=DIRECTION ( 'NONE',  ( 0.000000000000000000, 0.000000000000000000, -1.000000000000000000 ) ) ;
#8963=ORIENTED_EDGE ( 'NONE', *, *, #8737, .F. ) ;
#8976=VECTOR ( 'NONE', #7048, 1000.000000000000000 ) ;
#8981=FACE_OUTER_BOUND ( 'NONE', #4508, .T. ) ;
#8987=VERTEX_POINT ( 'NONE', #1732 ) ;
#8993=EDGE_CURVE ( 'NONE', #2280, #8784, #6163, .T. ) ;
#9003=DIRECTION ( 'NONE',  ( -1.000000000000000000, 0.000000000000000000, 0.000000000000000000 ) ) ;
#9029=DIRECTION ( 'NONE',  ( -0.000000000000000000, -1.000000000000000000, -0.000000000000000000 ) ) ;
#9051=DIRECTION ( 'NONE',  ( 0.000000000000000000, -1.000000000000000000, 0.000000000000000000 ) ) ;
#9078=DIRECTION ( 'NONE',  ( 0.000000000000000000, 0.000000000000000000, 1.000000000000000000 ) ) ;
#9082=CARTESIAN_POINT ( 'NONE',  ( -4.119968255444916849E-15, -3.500000000000000000, 0.000000000000000000 ) ) ;
#9086=CARTESIAN_POINT ( 'NONE',  ( 0.7500000000000000000, -2.750000000000002665, 1.500000000000000000 ) ) ;
#9090=( NAMED_UNIT ( * ) SI_UNIT ( $, .STERADIAN. ) SOLID_ANGLE_UNIT ( ) );
#9094=AXIS2_PLACEMENT_3D ( 'NONE', #6491, #1337, #7198 ) ;
#9099=LINE ( 'NONE', #8293, #5744 ) ;
#9106=DIRECTION ( 'NONE',  ( -0.000000000000000000, -0.000000000000000000, -1.000000000000000000 ) ) ;
#9107=CARTESIAN_POINT ( 'NONE',  ( -0.7500000000000000000, 0.7500000000000000000, 0.000000000000000000 ) ) ;
#9128=ORIENTED_EDGE ( 'NONE', *, *, #8346, .F. ) ;
#9132=DIRECTION ( 'NONE',  ( -0.000000000000000000, -0.000000000000000000, -1.000000000000000000 ) ) ;
#9135=SHAPE_REPRESENTATION_RELATIONSHIP ( 'NONE' , 'NONE' ,  #8501, #3701 ) ;
#9144=EDGE_CURVE ( 'NONE', #8767, #4339, #7780, .T. ) ;
#9178=VERTEX_POINT ( 'NONE', #2602 ) ;
#9181=EDGE_CURVE ( 'NONE', #6631, #2860, #1146, .T. ) ;
#9186=EDGE_LOOP ( 'NONE', ( #7833, #7142, #4421, #5959 ) ) ;
#9196=AXIS2_PLACEMENT_3D ( 'NONE', #4680, #1020, #6893 ) ;
#9200=DIRECTION ( 'NONE',  ( 1.000000000000000000, 0.000000000000000000, 0.000000000000000000 ) ) ;
#9209=VECTOR ( 'NONE', #3200, 999.9999999999998863 ) ;
#9211=DIRECTION ( 'NONE',  ( -0.7071067811865509034, -0.7071067811865442421, 0.000000000000000000 ) ) ;
#9213=PLANE ( 'NONE',  #2723 ) ;
#9219=ADVANCED_FACE ( 'NONE', ( #6149 ), #7948, .T. ) ;
#9238=CIRCLE ( 'NONE', #1733, 1.000000000000000000 ) ;
#9241=ORIENTED_EDGE ( 'NONE', *, *, #1335, .F. ) ;
#9252=ORIENTED_EDGE ( 'NONE', *, *, #3828, .T. ) ;
#9262=VERTEX_POINT ( 'NONE', #2586 ) ;
#9264=ORIENTED_EDGE ( 'NONE', *, *, #4245, .F. ) ;
#9267=LINE ( 'NONE', #7159, #5491 ) ;
#9281=DIRECTION ( 'NONE',  ( 0.000000000000000000, 0.000000000000000000, 1.000000000000000000 ) ) ;
#9288=DIRECTION ( 'NONE',  ( -0.000000000000000000, -0.000000000000000000, -1.000000000000000000 ) ) ;
#9300=VECTOR ( 'NONE', #7435, 999.9999999999998863 ) ;
#9309=ORIENTED_EDGE ( 'NONE', *, *, #6356, .F. ) ;
#9311=CONICAL_SURFACE ( 'NONE', #8861, 2.499999999999998668, 0.7853981633974461696 ) ;
#9319=DIRECTION ( 'NONE',  ( 0.000000000000000000, 0.000000000000000000, 1.000000000000000000 ) ) ;
#9351=CARTESIAN_POINT ( 'NONE',  ( 2.818925648462311528E-15, 3.500000000000000000, 0.000000000000000000 ) ) ;
#9384=CIRCLE ( 'NONE', #5253, 2.499999999999998668 ) ;
#9399=EDGE_CURVE ( 'NONE', #7970, #3755, #8534, .T. ) ;
#9402=EDGE_CURVE ( 'NONE', #2584, #6427, #8489, .T. ) ;
#9406=LINE ( 'NONE', #8014, #119 ) ;
#9444=LINE ( 'NONE', #702, #7635 ) ;
#9463=DIRECTION ( 'NONE',  ( 1.000000000000000000, 0.000000000000000000, -0.000000000000000000 ) ) ;
#9509=COLOUR_RGB('Light Blue',0.38,0.62,0.78);
#9510=FILL_AREA_STYLE_COLOUR('',#9509);
#9511=FILL_AREA_STYLE('',(#9510));
#9512=SURFACE_STYLE_FILL_AREA(#9511);
#9513=SURFACE_SIDE_STYLE('',(#9512));
#9514=SURFACE_STYLE_USAGE(.BOTH.,#9513);
#9515=PRESENTATION_STYLE_ASSIGNMENT((#9514));
ENDSEC;
END-ISO-10303-21;
